ISO-10303-21;
HEADER;
/* Generated by software containing ST-Developer
 * from STEP Tools, Inc. (www.steptools.com) 
 */

FILE_DESCRIPTION(
/* description */ ('Jaw-coupled motor to shaft test stand'),
/* implementation_level */ '2;1');

FILE_NAME(
/* name */ 'Cap Screw - M4x16.step',
/* time_stamp */ '2026-10-27T10:46:06-07:00',
/* author */ (''),
/* organization */ (''),
/* preprocessor_version */ 'ST-DEVELOPER v20.2',
/* originating_system */ 'Autodesk Translation Framework v15.17.0.0',
/* authorisation */ '');

FILE_SCHEMA (('AUTOMOTIVE_DESIGN { 1 0 10303 214 3 1 1 }'));
ENDSEC;

DATA;
#10=MECHANICAL_DESIGN_GEOMETRIC_PRESENTATION_REPRESENTATION('',(#372),#19361);
#25=CONICAL_SURFACE('',#12299,0.325,0.785398163397448);
#26=CONICAL_SURFACE('',#12303,0.335,0.785398163397448);
#27=CONICAL_SURFACE('',#12307,0.21,0.463647609000806);
#28=CONICAL_SURFACE('',#12311,0.18,0.785398163397448);
#31=ORIENTED_CLOSED_SHELL('',*,#11019,.F.);
#34=BREP_WITH_VOIDS('Body1',#11018,(#31));
#307=SHAPE_REPRESENTATION_RELATIONSHIP('SRR','None',#19524,#339);
#339=ADVANCED_BREP_SHAPE_REPRESENTATION('',(#34),#19360);
#372=STYLED_ITEM('',(#19753),#34);
#515=FACE_BOUND('',#2362,.T.);
#1011=PLANE('',#12297);
#1012=PLANE('',#12305);
#1013=PLANE('',#12313);
#1014=PLANE('',#12314);
#1015=PLANE('',#12315);
#1016=PLANE('',#12316);
#1017=PLANE('',#12317);
#1018=PLANE('',#12318);
#1019=PLANE('',#12319);
#1020=PLANE('',#12320);
#1021=PLANE('',#12321);
#1625=FACE_OUTER_BOUND('',#2357,.T.);
#1626=FACE_OUTER_BOUND('',#2358,.T.);
#1627=FACE_OUTER_BOUND('',#2359,.T.);
#1628=FACE_OUTER_BOUND('',#2360,.T.);
#1629=FACE_OUTER_BOUND('',#2361,.T.);
#1630=FACE_OUTER_BOUND('',#2363,.T.);
#1631=FACE_OUTER_BOUND('',#2364,.T.);
#1632=FACE_OUTER_BOUND('',#2365,.T.);
#1633=FACE_OUTER_BOUND('',#2366,.T.);
#1634=FACE_OUTER_BOUND('',#2367,.T.);
#1635=FACE_OUTER_BOUND('',#2368,.T.);
#1636=FACE_OUTER_BOUND('',#2369,.T.);
#1637=FACE_OUTER_BOUND('',#2370,.T.);
#1638=FACE_OUTER_BOUND('',#2371,.T.);
#1639=FACE_OUTER_BOUND('',#2372,.T.);
#1640=FACE_OUTER_BOUND('',#2373,.T.);
#1641=FACE_OUTER_BOUND('',#2374,.T.);
#2357=EDGE_LOOP('',(#10206));
#2358=EDGE_LOOP('',(#10207,#10208,#10209,#10210));
#2359=EDGE_LOOP('',(#10211,#10212,#10213,#10214));
#2360=EDGE_LOOP('',(#10215,#10216,#10217,#10218));
#2361=EDGE_LOOP('',(#10219));
#2362=EDGE_LOOP('',(#10220));
#2363=EDGE_LOOP('',(#10221,#10222,#10223,#10224));
#2364=EDGE_LOOP('',(#10225,#10226,#10227,#10228));
#2365=EDGE_LOOP('',(#10229,#10230,#10231,#10232));
#2366=EDGE_LOOP('',(#10233));
#2367=EDGE_LOOP('',(#10234,#10235,#10236,#10237));
#2368=EDGE_LOOP('',(#10238,#10239,#10240,#10241));
#2369=EDGE_LOOP('',(#10242,#10243,#10244,#10245));
#2370=EDGE_LOOP('',(#10246,#10247,#10248,#10249));
#2371=EDGE_LOOP('',(#10250,#10251,#10252,#10253));
#2372=EDGE_LOOP('',(#10254,#10255,#10256,#10257));
#2373=EDGE_LOOP('',(#10258,#10259,#10260,#10261,#10262,#10263));
#2374=EDGE_LOOP('',(#10264,#10265,#10266,#10267,#10268,#10269));
#3504=LINE('',#19205,#4657);
#3505=LINE('',#19209,#4658);
#3506=LINE('',#19213,#4659);
#3507=LINE('',#19220,#4660);
#3508=LINE('',#19224,#4661);
#3509=LINE('',#19228,#4662);
#3510=LINE('',#19233,#4663);
#3511=LINE('',#19235,#4664);
#3512=LINE('',#19237,#4665);
#3513=LINE('',#19238,#4666);
#3514=LINE('',#19241,#4667);
#3515=LINE('',#19243,#4668);
#3516=LINE('',#19244,#4669);
#3517=LINE('',#19247,#4670);
#3518=LINE('',#19249,#4671);
#3519=LINE('',#19250,#4672);
#3520=LINE('',#19253,#4673);
#3521=LINE('',#19255,#4674);
#3522=LINE('',#19256,#4675);
#3523=LINE('',#19259,#4676);
#3524=LINE('',#19261,#4677);
#3525=LINE('',#19262,#4678);
#3526=LINE('',#19264,#4679);
#3527=LINE('',#19265,#4680);
#4657=VECTOR('',#15325,0.325);
#4658=VECTOR('',#15330,0.35);
#4659=VECTOR('',#15335,0.335);
#4660=VECTOR('',#15344,0.21);
#4661=VECTOR('',#15349,0.2);
#4662=VECTOR('',#15354,0.18);
#4663=VECTOR('',#15359,1.);
#4664=VECTOR('',#15360,1.);
#4665=VECTOR('',#15361,1.);
#4666=VECTOR('',#15362,1.);
#4667=VECTOR('',#15365,1.);
#4668=VECTOR('',#15366,1.);
#4669=VECTOR('',#15367,1.);
#4670=VECTOR('',#15370,1.);
#4671=VECTOR('',#15371,1.);
#4672=VECTOR('',#15372,1.);
#4673=VECTOR('',#15375,1.);
#4674=VECTOR('',#15376,1.);
#4675=VECTOR('',#15377,1.);
#4676=VECTOR('',#15380,1.);
#4677=VECTOR('',#15381,1.);
#4678=VECTOR('',#15382,1.);
#4679=VECTOR('',#15385,1.);
#4680=VECTOR('',#15386,1.);
#4935=CIRCLE('',#12298,0.3);
#4936=CIRCLE('',#12300,0.35);
#4937=CIRCLE('',#12302,0.35);
#4938=CIRCLE('',#12304,0.32);
#4939=CIRCLE('',#12306,0.22);
#4940=CIRCLE('',#12308,0.1954);
#4941=CIRCLE('',#12310,0.1954);
#4942=CIRCLE('',#12312,0.16);
#5864=VERTEX_POINT('',#19200);
#5865=VERTEX_POINT('',#19203);
#5866=VERTEX_POINT('',#19207);
#5867=VERTEX_POINT('',#19211);
#5868=VERTEX_POINT('',#19215);
#5869=VERTEX_POINT('',#19218);
#5870=VERTEX_POINT('',#19222);
#5871=VERTEX_POINT('',#19226);
#5872=VERTEX_POINT('',#19231);
#5873=VERTEX_POINT('',#19232);
#5874=VERTEX_POINT('',#19234);
#5875=VERTEX_POINT('',#19236);
#5876=VERTEX_POINT('',#19240);
#5877=VERTEX_POINT('',#19242);
#5878=VERTEX_POINT('',#19246);
#5879=VERTEX_POINT('',#19248);
#5880=VERTEX_POINT('',#19252);
#5881=VERTEX_POINT('',#19254);
#5882=VERTEX_POINT('',#19258);
#5883=VERTEX_POINT('',#19260);
#7314=EDGE_CURVE('',#5864,#5864,#4935,.T.);
#7315=EDGE_CURVE('',#5865,#5865,#4936,.T.);
#7316=EDGE_CURVE('',#5865,#5864,#3504,.T.);
#7317=EDGE_CURVE('',#5866,#5866,#4937,.T.);
#7318=EDGE_CURVE('',#5866,#5865,#3505,.T.);
#7319=EDGE_CURVE('',#5867,#5867,#4938,.T.);
#7320=EDGE_CURVE('',#5867,#5866,#3506,.T.);
#7321=EDGE_CURVE('',#5868,#5868,#4939,.T.);
#7322=EDGE_CURVE('',#5869,#5869,#4940,.F.);
#7323=EDGE_CURVE('',#5869,#5868,#3507,.T.);
#7324=EDGE_CURVE('',#5870,#5870,#4941,.F.);
#7325=EDGE_CURVE('',#5870,#5869,#3508,.T.);
#7326=EDGE_CURVE('',#5871,#5871,#4942,.T.);
#7327=EDGE_CURVE('',#5871,#5870,#3509,.T.);
#7328=EDGE_CURVE('',#5872,#5873,#3510,.T.);
#7329=EDGE_CURVE('',#5873,#5874,#3511,.T.);
#7330=EDGE_CURVE('',#5874,#5875,#3512,.T.);
#7331=EDGE_CURVE('',#5872,#5875,#3513,.T.);
#7332=EDGE_CURVE('',#5873,#5876,#3514,.T.);
#7333=EDGE_CURVE('',#5876,#5877,#3515,.T.);
#7334=EDGE_CURVE('',#5877,#5874,#3516,.T.);
#7335=EDGE_CURVE('',#5876,#5878,#3517,.T.);
#7336=EDGE_CURVE('',#5878,#5879,#3518,.T.);
#7337=EDGE_CURVE('',#5879,#5877,#3519,.T.);
#7338=EDGE_CURVE('',#5878,#5880,#3520,.T.);
#7339=EDGE_CURVE('',#5880,#5881,#3521,.T.);
#7340=EDGE_CURVE('',#5881,#5879,#3522,.T.);
#7341=EDGE_CURVE('',#5880,#5882,#3523,.T.);
#7342=EDGE_CURVE('',#5882,#5883,#3524,.T.);
#7343=EDGE_CURVE('',#5883,#5881,#3525,.T.);
#7344=EDGE_CURVE('',#5882,#5872,#3526,.T.);
#7345=EDGE_CURVE('',#5875,#5883,#3527,.T.);
#10206=ORIENTED_EDGE('',*,*,#7314,.F.);
#10207=ORIENTED_EDGE('',*,*,#7315,.F.);
#10208=ORIENTED_EDGE('',*,*,#7316,.T.);
#10209=ORIENTED_EDGE('',*,*,#7314,.T.);
#10210=ORIENTED_EDGE('',*,*,#7316,.F.);
#10211=ORIENTED_EDGE('',*,*,#7317,.F.);
#10212=ORIENTED_EDGE('',*,*,#7318,.T.);
#10213=ORIENTED_EDGE('',*,*,#7315,.T.);
#10214=ORIENTED_EDGE('',*,*,#7318,.F.);
#10215=ORIENTED_EDGE('',*,*,#7319,.F.);
#10216=ORIENTED_EDGE('',*,*,#7320,.T.);
#10217=ORIENTED_EDGE('',*,*,#7317,.T.);
#10218=ORIENTED_EDGE('',*,*,#7320,.F.);
#10219=ORIENTED_EDGE('',*,*,#7319,.T.);
#10220=ORIENTED_EDGE('',*,*,#7321,.F.);
#10221=ORIENTED_EDGE('',*,*,#7322,.F.);
#10222=ORIENTED_EDGE('',*,*,#7323,.T.);
#10223=ORIENTED_EDGE('',*,*,#7321,.T.);
#10224=ORIENTED_EDGE('',*,*,#7323,.F.);
#10225=ORIENTED_EDGE('',*,*,#7324,.F.);
#10226=ORIENTED_EDGE('',*,*,#7325,.T.);
#10227=ORIENTED_EDGE('',*,*,#7322,.T.);
#10228=ORIENTED_EDGE('',*,*,#7325,.F.);
#10229=ORIENTED_EDGE('',*,*,#7326,.F.);
#10230=ORIENTED_EDGE('',*,*,#7327,.T.);
#10231=ORIENTED_EDGE('',*,*,#7324,.T.);
#10232=ORIENTED_EDGE('',*,*,#7327,.F.);
#10233=ORIENTED_EDGE('',*,*,#7326,.T.);
#10234=ORIENTED_EDGE('',*,*,#7328,.T.);
#10235=ORIENTED_EDGE('',*,*,#7329,.T.);
#10236=ORIENTED_EDGE('',*,*,#7330,.T.);
#10237=ORIENTED_EDGE('',*,*,#7331,.F.);
#10238=ORIENTED_EDGE('',*,*,#7332,.T.);
#10239=ORIENTED_EDGE('',*,*,#7333,.T.);
#10240=ORIENTED_EDGE('',*,*,#7334,.T.);
#10241=ORIENTED_EDGE('',*,*,#7329,.F.);
#10242=ORIENTED_EDGE('',*,*,#7335,.T.);
#10243=ORIENTED_EDGE('',*,*,#7336,.T.);
#10244=ORIENTED_EDGE('',*,*,#7337,.T.);
#10245=ORIENTED_EDGE('',*,*,#7333,.F.);
#10246=ORIENTED_EDGE('',*,*,#7338,.T.);
#10247=ORIENTED_EDGE('',*,*,#7339,.T.);
#10248=ORIENTED_EDGE('',*,*,#7340,.T.);
#10249=ORIENTED_EDGE('',*,*,#7336,.F.);
#10250=ORIENTED_EDGE('',*,*,#7341,.T.);
#10251=ORIENTED_EDGE('',*,*,#7342,.T.);
#10252=ORIENTED_EDGE('',*,*,#7343,.T.);
#10253=ORIENTED_EDGE('',*,*,#7339,.F.);
#10254=ORIENTED_EDGE('',*,*,#7344,.T.);
#10255=ORIENTED_EDGE('',*,*,#7331,.T.);
#10256=ORIENTED_EDGE('',*,*,#7345,.T.);
#10257=ORIENTED_EDGE('',*,*,#7342,.F.);
#10258=ORIENTED_EDGE('',*,*,#7344,.F.);
#10259=ORIENTED_EDGE('',*,*,#7341,.F.);
#10260=ORIENTED_EDGE('',*,*,#7338,.F.);
#10261=ORIENTED_EDGE('',*,*,#7335,.F.);
#10262=ORIENTED_EDGE('',*,*,#7332,.F.);
#10263=ORIENTED_EDGE('',*,*,#7328,.F.);
#10264=ORIENTED_EDGE('',*,*,#7345,.F.);
#10265=ORIENTED_EDGE('',*,*,#7330,.F.);
#10266=ORIENTED_EDGE('',*,*,#7334,.F.);
#10267=ORIENTED_EDGE('',*,*,#7337,.F.);
#10268=ORIENTED_EDGE('',*,*,#7340,.F.);
#10269=ORIENTED_EDGE('',*,*,#7343,.F.);
#10362=CYLINDRICAL_SURFACE('',#12301,0.35);
#10363=CYLINDRICAL_SURFACE('',#12309,0.1954);
#10967=ADVANCED_FACE('',(#1625),#1011,.T.);
#10968=ADVANCED_FACE('',(#1626),#25,.T.);
#10969=ADVANCED_FACE('',(#1627),#10362,.T.);
#10970=ADVANCED_FACE('',(#1628),#26,.T.);
#10971=ADVANCED_FACE('',(#1629,#515),#1012,.T.);
#10972=ADVANCED_FACE('',(#1630),#27,.T.);
#10973=ADVANCED_FACE('',(#1631),#10363,.T.);
#10974=ADVANCED_FACE('',(#1632),#28,.T.);
#10975=ADVANCED_FACE('',(#1633),#1013,.T.);
#10976=ADVANCED_FACE('',(#1634),#1014,.F.);
#10977=ADVANCED_FACE('',(#1635),#1015,.F.);
#10978=ADVANCED_FACE('',(#1636),#1016,.F.);
#10979=ADVANCED_FACE('',(#1637),#1017,.F.);
#10980=ADVANCED_FACE('',(#1638),#1018,.F.);
#10981=ADVANCED_FACE('',(#1639),#1019,.F.);
#10982=ADVANCED_FACE('',(#1640),#1020,.F.);
#10983=ADVANCED_FACE('',(#1641),#1021,.F.);
#11018=CLOSED_SHELL('',(#10967,#10968,#10969,#10970,#10971,#10972,#10973,
#10974,#10975));
#11019=CLOSED_SHELL('',(#10976,#10977,#10978,#10979,#10980,#10981,#10982,
#10983));
#12296=AXIS2_PLACEMENT_3D('',#19198,#15315,#15316);
#12297=AXIS2_PLACEMENT_3D('',#19199,#15317,#15318);
#12298=AXIS2_PLACEMENT_3D('',#19201,#15319,#15320);
#12299=AXIS2_PLACEMENT_3D('',#19202,#15321,#15322);
#12300=AXIS2_PLACEMENT_3D('',#19204,#15323,#15324);
#12301=AXIS2_PLACEMENT_3D('',#19206,#15326,#15327);
#12302=AXIS2_PLACEMENT_3D('',#19208,#15328,#15329);
#12303=AXIS2_PLACEMENT_3D('',#19210,#15331,#15332);
#12304=AXIS2_PLACEMENT_3D('',#19212,#15333,#15334);
#12305=AXIS2_PLACEMENT_3D('',#19214,#15336,#15337);
#12306=AXIS2_PLACEMENT_3D('',#19216,#15338,#15339);
#12307=AXIS2_PLACEMENT_3D('',#19217,#15340,#15341);
#12308=AXIS2_PLACEMENT_3D('',#19219,#15342,#15343);
#12309=AXIS2_PLACEMENT_3D('',#19221,#15345,#15346);
#12310=AXIS2_PLACEMENT_3D('',#19223,#15347,#15348);
#12311=AXIS2_PLACEMENT_3D('',#19225,#15350,#15351);
#12312=AXIS2_PLACEMENT_3D('',#19227,#15352,#15353);
#12313=AXIS2_PLACEMENT_3D('',#19229,#15355,#15356);
#12314=AXIS2_PLACEMENT_3D('',#19230,#15357,#15358);
#12315=AXIS2_PLACEMENT_3D('',#19239,#15363,#15364);
#12316=AXIS2_PLACEMENT_3D('',#19245,#15368,#15369);
#12317=AXIS2_PLACEMENT_3D('',#19251,#15373,#15374);
#12318=AXIS2_PLACEMENT_3D('',#19257,#15378,#15379);
#12319=AXIS2_PLACEMENT_3D('',#19263,#15383,#15384);
#12320=AXIS2_PLACEMENT_3D('',#19266,#15387,#15388);
#12321=AXIS2_PLACEMENT_3D('',#19267,#15389,#15390);
#15315=DIRECTION('axis',(0.,0.,1.));
#15316=DIRECTION('refdir',(1.,0.,0.));
#15317=DIRECTION('center_axis',(0.,1.,0.));
#15318=DIRECTION('ref_axis',(0.,0.,1.));
#15319=DIRECTION('center_axis',(0.,-1.,0.));
#15320=DIRECTION('ref_axis',(1.,0.,0.));
#15321=DIRECTION('center_axis',(0.,-1.,0.));
#15322=DIRECTION('ref_axis',(1.,0.,0.));
#15323=DIRECTION('center_axis',(0.,-1.,0.));
#15324=DIRECTION('ref_axis',(1.,0.,0.));
#15325=DIRECTION('',(0.707106781186547,0.707106781186548,8.65956056235493E-17));
#15326=DIRECTION('center_axis',(0.,-1.,0.));
#15327=DIRECTION('ref_axis',(1.,0.,0.));
#15328=DIRECTION('center_axis',(0.,-1.,0.));
#15329=DIRECTION('ref_axis',(1.,0.,0.));
#15330=DIRECTION('',(0.,1.,0.));
#15331=DIRECTION('center_axis',(0.,1.,0.));
#15332=DIRECTION('ref_axis',(1.,0.,0.));
#15333=DIRECTION('center_axis',(0.,-1.,0.));
#15334=DIRECTION('ref_axis',(1.,0.,0.));
#15335=DIRECTION('',(-0.707106781186547,0.707106781186548,-8.65956056235493E-17));
#15336=DIRECTION('center_axis',(0.,-1.,0.));
#15337=DIRECTION('ref_axis',(0.,0.,-1.));
#15338=DIRECTION('center_axis',(0.,-1.,0.));
#15339=DIRECTION('ref_axis',(1.,0.,0.));
#15340=DIRECTION('center_axis',(0.,1.,0.));
#15341=DIRECTION('ref_axis',(1.,0.,0.));
#15342=DIRECTION('center_axis',(0.,1.,0.));
#15343=DIRECTION('ref_axis',(1.,0.,0.));
#15344=DIRECTION('',(-0.447213595499958,0.894427190999916,-5.47678698264203E-17));
#15345=DIRECTION('center_axis',(0.,-1.,0.));
#15346=DIRECTION('ref_axis',(1.,0.,0.));
#15347=DIRECTION('center_axis',(0.,1.,0.));
#15348=DIRECTION('ref_axis',(1.,0.,0.));
#15349=DIRECTION('',(0.,1.,0.));
#15350=DIRECTION('center_axis',(0.,1.,0.));
#15351=DIRECTION('ref_axis',(1.,0.,0.));
#15352=DIRECTION('center_axis',(0.,-1.,0.));
#15353=DIRECTION('ref_axis',(1.,0.,0.));
#15354=DIRECTION('',(-0.707106781186547,0.707106781186548,-8.65956056235493E-17));
#15355=DIRECTION('center_axis',(0.,-1.,0.));
#15356=DIRECTION('ref_axis',(0.,0.,-1.));
#15357=DIRECTION('center_axis',(0.866025403784439,0.,-0.5));
#15358=DIRECTION('ref_axis',(0.5,0.,0.866025403784439));
#15359=DIRECTION('',(-0.5,0.,-0.866025403784439));
#15360=DIRECTION('',(0.,-1.,0.));
#15361=DIRECTION('',(0.5,0.,0.866025403784439));
#15362=DIRECTION('',(0.,-1.,0.));
#15363=DIRECTION('center_axis',(1.60246890531964E-16,0.,-1.));
#15364=DIRECTION('ref_axis',(1.,0.,1.60246890531964E-16));
#15365=DIRECTION('',(-1.,0.,-1.60246890531964E-16));
#15366=DIRECTION('',(0.,-1.,0.));
#15367=DIRECTION('',(1.,0.,1.60246890531964E-16));
#15368=DIRECTION('center_axis',(-0.866025403784439,0.,-0.5));
#15369=DIRECTION('ref_axis',(0.5,0.,-0.866025403784439));
#15370=DIRECTION('',(-0.5,0.,0.866025403784439));
#15371=DIRECTION('',(0.,-1.,0.));
#15372=DIRECTION('',(0.5,0.,-0.866025403784439));
#15373=DIRECTION('center_axis',(-0.866025403784439,0.,0.5));
#15374=DIRECTION('ref_axis',(-0.5,0.,-0.866025403784439));
#15375=DIRECTION('',(0.5,0.,0.866025403784439));
#15376=DIRECTION('',(0.,-1.,0.));
#15377=DIRECTION('',(-0.5,0.,-0.866025403784439));
#15378=DIRECTION('center_axis',(-1.60246890531964E-16,0.,1.));
#15379=DIRECTION('ref_axis',(-1.,0.,-1.60246890531964E-16));
#15380=DIRECTION('',(1.,0.,1.60246890531964E-16));
#15381=DIRECTION('',(0.,-1.,0.));
#15382=DIRECTION('',(-1.,0.,-1.60246890531964E-16));
#15383=DIRECTION('center_axis',(0.866025403784439,0.,0.5));
#15384=DIRECTION('ref_axis',(-0.5,0.,0.866025403784439));
#15385=DIRECTION('',(0.5,0.,-0.866025403784439));
#15386=DIRECTION('',(-0.5,0.,0.866025403784439));
#15387=DIRECTION('center_axis',(0.,1.,0.));
#15388=DIRECTION('ref_axis',(1.,0.,0.));
#15389=DIRECTION('center_axis',(0.,-1.,0.));
#15390=DIRECTION('ref_axis',(0.,0.,-1.));
#19198=CARTESIAN_POINT('',(0.,0.,0.));
#19199=CARTESIAN_POINT('Origin',(0.3,0.4,0.));
#19200=CARTESIAN_POINT('',(-0.3,0.4,-3.67394039744206E-17));
#19201=CARTESIAN_POINT('Origin',(0.,0.4,0.));
#19202=CARTESIAN_POINT('Origin',(0.,0.375,0.));
#19203=CARTESIAN_POINT('',(-0.35,0.35,-4.28626379701573E-17));
#19204=CARTESIAN_POINT('Origin',(0.,0.35,0.));
#19205=CARTESIAN_POINT('',(-0.325,0.375,-3.9801020972289E-17));
#19206=CARTESIAN_POINT('Origin',(0.,0.19,0.));
#19207=CARTESIAN_POINT('',(-0.35,0.03,-4.28626379701574E-17));
#19208=CARTESIAN_POINT('Origin',(0.,0.03,0.));
#19209=CARTESIAN_POINT('',(-0.35,0.19,-4.28626379701574E-17));
#19210=CARTESIAN_POINT('Origin',(0.,0.0149999999999999,0.));
#19211=CARTESIAN_POINT('',(-0.32,-3.29597460435593E-17,-3.91886975727153E-17));
#19212=CARTESIAN_POINT('Origin',(0.,0.,0.));
#19213=CARTESIAN_POINT('',(-0.335,0.0149999999999999,-4.10256677714363E-17));
#19214=CARTESIAN_POINT('Origin',(0.22,0.,0.));
#19215=CARTESIAN_POINT('',(-0.22,-6.93889390390723E-18,-2.69422295812418E-17));
#19216=CARTESIAN_POINT('Origin',(0.,0.,0.));
#19217=CARTESIAN_POINT('Origin',(0.,-0.02,0.));
#19218=CARTESIAN_POINT('',(-0.1954,-0.0492,2.39295984553393E-17));
#19219=CARTESIAN_POINT('Origin',(0.,-0.0492,0.));
#19220=CARTESIAN_POINT('',(-0.21,-0.02,-2.57175827820944E-17));
#19221=CARTESIAN_POINT('Origin',(0.,-0.8,0.));
#19222=CARTESIAN_POINT('',(-0.1954,-1.5646,2.39295984553393E-17));
#19223=CARTESIAN_POINT('Origin',(0.,-1.5646,0.));
#19224=CARTESIAN_POINT('',(-0.1954,-0.8,-2.39295984553393E-17));
#19225=CARTESIAN_POINT('Origin',(0.,-1.58,0.));
#19226=CARTESIAN_POINT('',(-0.16,-1.6,-1.95943487863577E-17));
#19227=CARTESIAN_POINT('Origin',(0.,-1.6,0.));
#19228=CARTESIAN_POINT('',(-0.18,-1.58,-2.20436423846524E-17));
#19229=CARTESIAN_POINT('Origin',(0.,-1.6,0.));
#19230=CARTESIAN_POINT('Origin',(0.0866025403784439,-0.4,-0.15));
#19231=CARTESIAN_POINT('',(0.173205080756888,-0.4,0.));
#19232=CARTESIAN_POINT('',(0.0866025403784439,-0.4,-0.15));
#19233=CARTESIAN_POINT('',(0.173205080756888,-0.4,0.));
#19234=CARTESIAN_POINT('',(0.0866025403784439,-0.64,-0.15));
#19235=CARTESIAN_POINT('',(0.0866025403784439,-0.4,-0.15));
#19236=CARTESIAN_POINT('',(0.173205080756888,-0.64,0.));
#19237=CARTESIAN_POINT('',(0.173205080756888,-0.64,0.));
#19238=CARTESIAN_POINT('',(0.173205080756888,-0.4,0.));
#19239=CARTESIAN_POINT('Origin',(-0.0866025403784438,-0.4,-0.15));
#19240=CARTESIAN_POINT('',(-0.0866025403784438,-0.4,-0.15));
#19241=CARTESIAN_POINT('',(0.0866025403784439,-0.4,-0.15));
#19242=CARTESIAN_POINT('',(-0.0866025403784438,-0.64,-0.15));
#19243=CARTESIAN_POINT('',(-0.0866025403784438,-0.4,-0.15));
#19244=CARTESIAN_POINT('',(0.0866025403784439,-0.64,-0.15));
#19245=CARTESIAN_POINT('Origin',(-0.173205080756888,-0.4,-2.77555756156289E-17));
#19246=CARTESIAN_POINT('',(-0.173205080756888,-0.4,-2.12115047744981E-17));
#19247=CARTESIAN_POINT('',(-0.0866025403784438,-0.4,-0.15));
#19248=CARTESIAN_POINT('',(-0.173205080756888,-0.64,-2.77555756156289E-17));
#19249=CARTESIAN_POINT('',(-0.173205080756888,-0.4,-2.12115047744981E-17));
#19250=CARTESIAN_POINT('',(-0.0866025403784438,-0.64,-0.15));
#19251=CARTESIAN_POINT('Origin',(-0.0866025403784439,-0.4,0.15));
#19252=CARTESIAN_POINT('',(-0.0866025403784439,-0.4,0.15));
#19253=CARTESIAN_POINT('',(-0.173205080756888,-0.4,-2.12115047744981E-17));
#19254=CARTESIAN_POINT('',(-0.0866025403784439,-0.64,0.15));
#19255=CARTESIAN_POINT('',(-0.0866025403784439,-0.4,0.15));
#19256=CARTESIAN_POINT('',(-0.173205080756888,-0.64,-2.12115047744981E-17));
#19257=CARTESIAN_POINT('Origin',(0.0866025403784439,-0.4,0.15));
#19258=CARTESIAN_POINT('',(0.0866025403784439,-0.4,0.15));
#19259=CARTESIAN_POINT('',(-0.0866025403784439,-0.4,0.15));
#19260=CARTESIAN_POINT('',(0.0866025403784439,-0.64,0.15));
#19261=CARTESIAN_POINT('',(0.0866025403784439,-0.4,0.15));
#19262=CARTESIAN_POINT('',(-0.0866025403784439,-0.64,0.15));
#19263=CARTESIAN_POINT('Origin',(0.173205080756888,-0.4,0.));
#19264=CARTESIAN_POINT('',(0.0866025403784439,-0.4,0.15));
#19265=CARTESIAN_POINT('',(0.0866025403784439,-0.64,0.15));
#19266=CARTESIAN_POINT('Origin',(0.,-0.4,-2.77555756156289E-17));
#19267=CARTESIAN_POINT('Origin',(0.,-0.64,-2.77555756156289E-17));
#19322=UNCERTAINTY_MEASURE_WITH_UNIT(LENGTH_MEASURE(0.001),#19362,
'DISTANCE_ACCURACY_VALUE',
'Maximum model space distance between geometric entities at asserted c
onnectivities');
#19323=UNCERTAINTY_MEASURE_WITH_UNIT(LENGTH_MEASURE(0.001),#19362,
'DISTANCE_ACCURACY_VALUE',
'Maximum model space distance between geometric entities at asserted c
onnectivities');
#19360=(
GEOMETRIC_REPRESENTATION_CONTEXT(3)
GLOBAL_UNCERTAINTY_ASSIGNED_CONTEXT((#19322))
GLOBAL_UNIT_ASSIGNED_CONTEXT((#19362,#19364,#19365))
REPRESENTATION_CONTEXT('','3D')
);
#19361=(
GEOMETRIC_REPRESENTATION_CONTEXT(3)
GLOBAL_UNCERTAINTY_ASSIGNED_CONTEXT((#19323))
GLOBAL_UNIT_ASSIGNED_CONTEXT((#19362,#19364,#19365))
REPRESENTATION_CONTEXT('','3D')
);
#19362=(
LENGTH_UNIT()
NAMED_UNIT(*)
SI_UNIT(.CENTI.,.METRE.)
);
#19364=(
NAMED_UNIT(*)
PLANE_ANGLE_UNIT()
SI_UNIT($,.RADIAN.)
);
#19365=(
NAMED_UNIT(*)
SI_UNIT($,.STERADIAN.)
SOLID_ANGLE_UNIT()
);
#19402=SHAPE_DEFINITION_REPRESENTATION(#19469,#19524);
#19469=PRODUCT_DEFINITION_SHAPE('',$,#19562);
#19524=SHAPE_REPRESENTATION('',(#12296),#19360);
#19525=PRODUCT_DEFINITION_CONTEXT('part definition',#19638,'design');
#19562=PRODUCT_DEFINITION('Cap Screw - M4x16','Cap Screw - M4x16',#19599,
#19525);
#19599=PRODUCT_DEFINITION_FORMATION('',$,#19676);
#19638=APPLICATION_CONTEXT(
'Core Data for Automotive Mechanical Design Process');
#19639=PRODUCT_CONTEXT('part definition',#19638,'mechanical');
#19676=PRODUCT('Cap Screw - M4x16','Cap Screw - M4x16',
'Cap Screw - M4x16',(#19639));
#19747=COLOUR_RGB('Black',0.12,0.14,0.17);
#19748=FILL_AREA_STYLE_COLOUR('',#19747);
#19749=FILL_AREA_STYLE('',(#19748));
#19750=SURFACE_STYLE_FILL_AREA(#19749);
#19751=SURFACE_SIDE_STYLE('',(#19750));
#19752=SURFACE_STYLE_USAGE(.BOTH.,#19751);
#19753=PRESENTATION_STYLE_ASSIGNMENT((#19752));
ENDSEC;
END-ISO-10303-21;
